ISO-10303-21;
HEADER;
/* Generated by software containing ST-Developer
 * from STEP Tools, Inc. (www.steptools.com) 
 */

FILE_DESCRIPTION(
/* description */ ('Chute with adjustable gate'),
/* implementation_level */ '2;1');

FILE_NAME(
/* name */ 'Captive slot nut.step',
/* time_stamp */ '2026-10-27T10:52:28-07:00',
/* author */ (''),
/* organization */ (''),
/* preprocessor_version */ 'ST-DEVELOPER v20.2',
/* originating_system */ 'Autodesk Translation Framework v15.17.0.0',
/* authorisation */ '');

FILE_SCHEMA (('AUTOMOTIVE_DESIGN { 1 0 10303 214 3 1 1 }'));
ENDSEC;

DATA;
#10=MECHANICAL_DESIGN_GEOMETRIC_PRESENTATION_REPRESENTATION('',(#436),#13094);
#323=ELLIPSE('',#8401,0.299389011154384,0.2117);
#324=ELLIPSE('',#8405,0.299389011154384,0.2117);
#372=SHAPE_REPRESENTATION_RELATIONSHIP('SRR','None',#13273,#404);
#404=ADVANCED_BREP_SHAPE_REPRESENTATION('',(#467),#13082);
#436=STYLED_ITEM('',(#13502),#467);
#467=MANIFOLD_SOLID_BREP('Body1',#7620);
#565=FACE_BOUND('',#1697,.T.);
#809=PLANE('',#8391);
#810=PLANE('',#8392);
#811=PLANE('',#8393);
#812=PLANE('',#8395);
#813=PLANE('',#8396);
#814=PLANE('',#8397);
#815=PLANE('',#8398);
#816=PLANE('',#8399);
#817=PLANE('',#8400);
#818=PLANE('',#8407);
#819=PLANE('',#8408);
#820=PLANE('',#8409);
#821=PLANE('',#8410);
#1188=FACE_OUTER_BOUND('',#1694,.T.);
#1189=FACE_OUTER_BOUND('',#1695,.T.);
#1190=FACE_OUTER_BOUND('',#1696,.T.);
#1191=FACE_OUTER_BOUND('',#1698,.T.);
#1192=FACE_OUTER_BOUND('',#1699,.T.);
#1193=FACE_OUTER_BOUND('',#1700,.T.);
#1194=FACE_OUTER_BOUND('',#1701,.T.);
#1195=FACE_OUTER_BOUND('',#1702,.T.);
#1196=FACE_OUTER_BOUND('',#1703,.T.);
#1197=FACE_OUTER_BOUND('',#1704,.T.);
#1198=FACE_OUTER_BOUND('',#1705,.T.);
#1199=FACE_OUTER_BOUND('',#1706,.T.);
#1200=FACE_OUTER_BOUND('',#1707,.T.);
#1201=FACE_OUTER_BOUND('',#1708,.T.);
#1694=EDGE_LOOP('',(#6456,#6457,#6458,#6459));
#1695=EDGE_LOOP('',(#6460,#6461,#6462,#6463));
#1696=EDGE_LOOP('',(#6464,#6465,#6466,#6467));
#1697=EDGE_LOOP('',(#6468));
#1698=EDGE_LOOP('',(#6469,#6470,#6471,#6472,#6473,#6474,#6475,#6476,#6477,
#6478));
#1699=EDGE_LOOP('',(#6479,#6480,#6481,#6482));
#1700=EDGE_LOOP('',(#6483,#6484,#6485,#6486));
#1701=EDGE_LOOP('',(#6487,#6488,#6489,#6490,#6491,#6492,#6493,#6494,#6495,
#6496));
#1702=EDGE_LOOP('',(#6497,#6498,#6499,#6500));
#1703=EDGE_LOOP('',(#6501,#6502,#6503,#6504,#6505,#6506));
#1704=EDGE_LOOP('',(#6507,#6508,#6509,#6510,#6511,#6512,#6513,#6514));
#1705=EDGE_LOOP('',(#6515,#6516,#6517,#6518,#6519));
#1706=EDGE_LOOP('',(#6520,#6521,#6522,#6523));
#1707=EDGE_LOOP('',(#6524,#6525,#6526,#6527,#6528,#6529));
#1708=EDGE_LOOP('',(#6530,#6531,#6532,#6533));
#2389=LINE('',#12258,#3166);
#2390=LINE('',#12260,#3167);
#2391=LINE('',#12262,#3168);
#2392=LINE('',#12263,#3169);
#2393=LINE('',#12266,#3170);
#2394=LINE('',#12268,#3171);
#2395=LINE('',#12269,#3172);
#2396=LINE('',#12272,#3173);
#2397=LINE('',#12274,#3174);
#2398=LINE('',#12275,#3175);
#2399=LINE('',#12280,#3176);
#2400=LINE('',#12282,#3177);
#2401=LINE('',#12284,#3178);
#2402=LINE('',#12286,#3179);
#2403=LINE('',#12288,#3180);
#2404=LINE('',#12290,#3181);
#2405=LINE('',#12291,#3182);
#2406=LINE('',#12294,#3183);
#2407=LINE('',#12295,#3184);
#2408=LINE('',#12298,#3185);
#2409=LINE('',#12299,#3186);
#2410=LINE('',#12302,#3187);
#2411=LINE('',#12304,#3188);
#2412=LINE('',#12306,#3189);
#2413=LINE('',#12308,#3190);
#2414=LINE('',#12309,#3191);
#2415=LINE('',#12311,#3192);
#2416=LINE('',#12314,#3193);
#2417=LINE('',#12317,#3194);
#2418=LINE('',#12321,#3195);
#2419=LINE('',#12328,#3196);
#2420=LINE('',#12330,#3197);
#2421=LINE('',#12332,#3198);
#3166=VECTOR('',#10039,1.);
#3167=VECTOR('',#10040,1.);
#3168=VECTOR('',#10041,1.);
#3169=VECTOR('',#10042,1.);
#3170=VECTOR('',#10045,1.);
#3171=VECTOR('',#10046,1.);
#3172=VECTOR('',#10047,1.);
#3173=VECTOR('',#10050,1.);
#3174=VECTOR('',#10051,1.);
#3175=VECTOR('',#10052,1.);
#3176=VECTOR('',#10057,1.);
#3177=VECTOR('',#10058,1.);
#3178=VECTOR('',#10059,1.);
#3179=VECTOR('',#10060,1.);
#3180=VECTOR('',#10061,1.);
#3181=VECTOR('',#10062,1.);
#3182=VECTOR('',#10063,1.);
#3183=VECTOR('',#10066,1.);
#3184=VECTOR('',#10067,1.);
#3185=VECTOR('',#10070,1.);
#3186=VECTOR('',#10071,1.);
#3187=VECTOR('',#10074,1.);
#3188=VECTOR('',#10075,1.);
#3189=VECTOR('',#10076,1.);
#3190=VECTOR('',#10077,1.);
#3191=VECTOR('',#10078,1.);
#3192=VECTOR('',#10081,1.);
#3193=VECTOR('',#10084,1.);
#3194=VECTOR('',#10087,1.);
#3195=VECTOR('',#10092,0.21);
#3196=VECTOR('',#10101,1.);
#3197=VECTOR('',#10104,1.);
#3198=VECTOR('',#10107,1.);
#3520=CIRCLE('',#8394,0.2117);
#3521=CIRCLE('',#8403,0.2117);
#3522=CIRCLE('',#8404,0.2117);
#3523=CIRCLE('',#8406,0.2117);
#4015=VERTEX_POINT('',#12256);
#4016=VERTEX_POINT('',#12257);
#4017=VERTEX_POINT('',#12259);
#4018=VERTEX_POINT('',#12261);
#4019=VERTEX_POINT('',#12265);
#4020=VERTEX_POINT('',#12267);
#4021=VERTEX_POINT('',#12271);
#4022=VERTEX_POINT('',#12273);
#4023=VERTEX_POINT('',#12276);
#4024=VERTEX_POINT('',#12279);
#4025=VERTEX_POINT('',#12281);
#4026=VERTEX_POINT('',#12283);
#4027=VERTEX_POINT('',#12285);
#4028=VERTEX_POINT('',#12287);
#4029=VERTEX_POINT('',#12289);
#4030=VERTEX_POINT('',#12293);
#4031=VERTEX_POINT('',#12297);
#4032=VERTEX_POINT('',#12301);
#4033=VERTEX_POINT('',#12303);
#4034=VERTEX_POINT('',#12305);
#4035=VERTEX_POINT('',#12307);
#4036=VERTEX_POINT('',#12313);
#4037=VERTEX_POINT('',#12315);
#4038=VERTEX_POINT('',#12319);
#4039=VERTEX_POINT('',#12322);
#4040=VERTEX_POINT('',#12324);
#4861=EDGE_CURVE('',#4015,#4016,#2389,.T.);
#4862=EDGE_CURVE('',#4017,#4015,#2390,.T.);
#4863=EDGE_CURVE('',#4018,#4017,#2391,.T.);
#4864=EDGE_CURVE('',#4016,#4018,#2392,.T.);
#4865=EDGE_CURVE('',#4017,#4019,#2393,.T.);
#4866=EDGE_CURVE('',#4020,#4019,#2394,.T.);
#4867=EDGE_CURVE('',#4018,#4020,#2395,.T.);
#4868=EDGE_CURVE('',#4019,#4021,#2396,.T.);
#4869=EDGE_CURVE('',#4021,#4022,#2397,.T.);
#4870=EDGE_CURVE('',#4022,#4020,#2398,.T.);
#4871=EDGE_CURVE('',#4023,#4023,#3520,.T.);
#4872=EDGE_CURVE('',#4024,#4015,#2399,.T.);
#4873=EDGE_CURVE('',#4025,#4024,#2400,.T.);
#4874=EDGE_CURVE('',#4025,#4026,#2401,.T.);
#4875=EDGE_CURVE('',#4027,#4026,#2402,.T.);
#4876=EDGE_CURVE('',#4027,#4028,#2403,.T.);
#4877=EDGE_CURVE('',#4028,#4029,#2404,.T.);
#4878=EDGE_CURVE('',#4029,#4021,#2405,.T.);
#4879=EDGE_CURVE('',#4029,#4030,#2406,.T.);
#4880=EDGE_CURVE('',#4030,#4022,#2407,.T.);
#4881=EDGE_CURVE('',#4031,#4028,#2408,.T.);
#4882=EDGE_CURVE('',#4030,#4031,#2409,.T.);
#4883=EDGE_CURVE('',#4032,#4031,#2410,.T.);
#4884=EDGE_CURVE('',#4033,#4032,#2411,.T.);
#4885=EDGE_CURVE('',#4033,#4034,#2412,.T.);
#4886=EDGE_CURVE('',#4035,#4034,#2413,.T.);
#4887=EDGE_CURVE('',#4035,#4016,#2414,.T.);
#4888=EDGE_CURVE('',#4032,#4027,#2415,.T.);
#4889=EDGE_CURVE('',#4026,#4036,#2416,.T.);
#4890=EDGE_CURVE('',#4036,#4037,#323,.T.);
#4891=EDGE_CURVE('',#4037,#4033,#2417,.T.);
#4892=EDGE_CURVE('',#4038,#4036,#3521,.F.);
#4893=EDGE_CURVE('',#4038,#4023,#2418,.T.);
#4894=EDGE_CURVE('',#4039,#4038,#3522,.F.);
#4895=EDGE_CURVE('',#4040,#4039,#324,.T.);
#4896=EDGE_CURVE('',#4037,#4040,#3523,.F.);
#4897=EDGE_CURVE('',#4039,#4025,#2419,.T.);
#4898=EDGE_CURVE('',#4034,#4040,#2420,.T.);
#4899=EDGE_CURVE('',#4024,#4035,#2421,.T.);
#6456=ORIENTED_EDGE('',*,*,#4861,.F.);
#6457=ORIENTED_EDGE('',*,*,#4862,.F.);
#6458=ORIENTED_EDGE('',*,*,#4863,.F.);
#6459=ORIENTED_EDGE('',*,*,#4864,.F.);
#6460=ORIENTED_EDGE('',*,*,#4863,.T.);
#6461=ORIENTED_EDGE('',*,*,#4865,.T.);
#6462=ORIENTED_EDGE('',*,*,#4866,.F.);
#6463=ORIENTED_EDGE('',*,*,#4867,.F.);
#6464=ORIENTED_EDGE('',*,*,#4868,.T.);
#6465=ORIENTED_EDGE('',*,*,#4869,.T.);
#6466=ORIENTED_EDGE('',*,*,#4870,.T.);
#6467=ORIENTED_EDGE('',*,*,#4866,.T.);
#6468=ORIENTED_EDGE('',*,*,#4871,.T.);
#6469=ORIENTED_EDGE('',*,*,#4868,.F.);
#6470=ORIENTED_EDGE('',*,*,#4865,.F.);
#6471=ORIENTED_EDGE('',*,*,#4862,.T.);
#6472=ORIENTED_EDGE('',*,*,#4872,.F.);
#6473=ORIENTED_EDGE('',*,*,#4873,.F.);
#6474=ORIENTED_EDGE('',*,*,#4874,.T.);
#6475=ORIENTED_EDGE('',*,*,#4875,.F.);
#6476=ORIENTED_EDGE('',*,*,#4876,.T.);
#6477=ORIENTED_EDGE('',*,*,#4877,.T.);
#6478=ORIENTED_EDGE('',*,*,#4878,.T.);
#6479=ORIENTED_EDGE('',*,*,#4879,.T.);
#6480=ORIENTED_EDGE('',*,*,#4880,.T.);
#6481=ORIENTED_EDGE('',*,*,#4869,.F.);
#6482=ORIENTED_EDGE('',*,*,#4878,.F.);
#6483=ORIENTED_EDGE('',*,*,#4881,.F.);
#6484=ORIENTED_EDGE('',*,*,#4882,.F.);
#6485=ORIENTED_EDGE('',*,*,#4879,.F.);
#6486=ORIENTED_EDGE('',*,*,#4877,.F.);
#6487=ORIENTED_EDGE('',*,*,#4870,.F.);
#6488=ORIENTED_EDGE('',*,*,#4880,.F.);
#6489=ORIENTED_EDGE('',*,*,#4882,.T.);
#6490=ORIENTED_EDGE('',*,*,#4883,.F.);
#6491=ORIENTED_EDGE('',*,*,#4884,.F.);
#6492=ORIENTED_EDGE('',*,*,#4885,.T.);
#6493=ORIENTED_EDGE('',*,*,#4886,.F.);
#6494=ORIENTED_EDGE('',*,*,#4887,.T.);
#6495=ORIENTED_EDGE('',*,*,#4864,.T.);
#6496=ORIENTED_EDGE('',*,*,#4867,.T.);
#6497=ORIENTED_EDGE('',*,*,#4881,.T.);
#6498=ORIENTED_EDGE('',*,*,#4876,.F.);
#6499=ORIENTED_EDGE('',*,*,#4888,.F.);
#6500=ORIENTED_EDGE('',*,*,#4883,.T.);
#6501=ORIENTED_EDGE('',*,*,#4884,.T.);
#6502=ORIENTED_EDGE('',*,*,#4888,.T.);
#6503=ORIENTED_EDGE('',*,*,#4875,.T.);
#6504=ORIENTED_EDGE('',*,*,#4889,.T.);
#6505=ORIENTED_EDGE('',*,*,#4890,.T.);
#6506=ORIENTED_EDGE('',*,*,#4891,.T.);
#6507=ORIENTED_EDGE('',*,*,#4890,.F.);
#6508=ORIENTED_EDGE('',*,*,#4892,.F.);
#6509=ORIENTED_EDGE('',*,*,#4893,.T.);
#6510=ORIENTED_EDGE('',*,*,#4871,.F.);
#6511=ORIENTED_EDGE('',*,*,#4893,.F.);
#6512=ORIENTED_EDGE('',*,*,#4894,.F.);
#6513=ORIENTED_EDGE('',*,*,#4895,.F.);
#6514=ORIENTED_EDGE('',*,*,#4896,.F.);
#6515=ORIENTED_EDGE('',*,*,#4889,.F.);
#6516=ORIENTED_EDGE('',*,*,#4874,.F.);
#6517=ORIENTED_EDGE('',*,*,#4897,.F.);
#6518=ORIENTED_EDGE('',*,*,#4894,.T.);
#6519=ORIENTED_EDGE('',*,*,#4892,.T.);
#6520=ORIENTED_EDGE('',*,*,#4891,.F.);
#6521=ORIENTED_EDGE('',*,*,#4896,.T.);
#6522=ORIENTED_EDGE('',*,*,#4898,.F.);
#6523=ORIENTED_EDGE('',*,*,#4885,.F.);
#6524=ORIENTED_EDGE('',*,*,#4873,.T.);
#6525=ORIENTED_EDGE('',*,*,#4899,.T.);
#6526=ORIENTED_EDGE('',*,*,#4886,.T.);
#6527=ORIENTED_EDGE('',*,*,#4898,.T.);
#6528=ORIENTED_EDGE('',*,*,#4895,.T.);
#6529=ORIENTED_EDGE('',*,*,#4897,.T.);
#6530=ORIENTED_EDGE('',*,*,#4861,.T.);
#6531=ORIENTED_EDGE('',*,*,#4887,.F.);
#6532=ORIENTED_EDGE('',*,*,#4899,.F.);
#6533=ORIENTED_EDGE('',*,*,#4872,.T.);
#7157=CYLINDRICAL_SURFACE('',#8402,0.2117);
#7456=ADVANCED_FACE('',(#1188),#809,.F.);
#7457=ADVANCED_FACE('',(#1189),#810,.T.);
#7458=ADVANCED_FACE('',(#1190,#565),#811,.T.);
#7459=ADVANCED_FACE('',(#1191),#812,.T.);
#7460=ADVANCED_FACE('',(#1192),#813,.T.);
#7461=ADVANCED_FACE('',(#1193),#814,.F.);
#7462=ADVANCED_FACE('',(#1194),#815,.T.);
#7463=ADVANCED_FACE('',(#1195),#816,.T.);
#7464=ADVANCED_FACE('',(#1196),#817,.T.);
#7465=ADVANCED_FACE('',(#1197),#7157,.F.);
#7466=ADVANCED_FACE('',(#1198),#818,.F.);
#7467=ADVANCED_FACE('',(#1199),#819,.F.);
#7468=ADVANCED_FACE('',(#1200),#820,.T.);
#7469=ADVANCED_FACE('',(#1201),#821,.T.);
#7620=CLOSED_SHELL('',(#7456,#7457,#7458,#7459,#7460,#7461,#7462,#7463,
#7464,#7465,#7466,#7467,#7468,#7469));
#8390=AXIS2_PLACEMENT_3D('',#12254,#10035,#10036);
#8391=AXIS2_PLACEMENT_3D('',#12255,#10037,#10038);
#8392=AXIS2_PLACEMENT_3D('',#12264,#10043,#10044);
#8393=AXIS2_PLACEMENT_3D('',#12270,#10048,#10049);
#8394=AXIS2_PLACEMENT_3D('',#12277,#10053,#10054);
#8395=AXIS2_PLACEMENT_3D('',#12278,#10055,#10056);
#8396=AXIS2_PLACEMENT_3D('',#12292,#10064,#10065);
#8397=AXIS2_PLACEMENT_3D('',#12296,#10068,#10069);
#8398=AXIS2_PLACEMENT_3D('',#12300,#10072,#10073);
#8399=AXIS2_PLACEMENT_3D('',#12310,#10079,#10080);
#8400=AXIS2_PLACEMENT_3D('',#12312,#10082,#10083);
#8401=AXIS2_PLACEMENT_3D('',#12316,#10085,#10086);
#8402=AXIS2_PLACEMENT_3D('',#12318,#10088,#10089);
#8403=AXIS2_PLACEMENT_3D('',#12320,#10090,#10091);
#8404=AXIS2_PLACEMENT_3D('',#12323,#10093,#10094);
#8405=AXIS2_PLACEMENT_3D('',#12325,#10095,#10096);
#8406=AXIS2_PLACEMENT_3D('',#12326,#10097,#10098);
#8407=AXIS2_PLACEMENT_3D('',#12327,#10099,#10100);
#8408=AXIS2_PLACEMENT_3D('',#12329,#10102,#10103);
#8409=AXIS2_PLACEMENT_3D('',#12331,#10105,#10106);
#8410=AXIS2_PLACEMENT_3D('',#12333,#10108,#10109);
#10035=DIRECTION('axis',(0.,0.,1.));
#10036=DIRECTION('refdir',(1.,0.,0.));
#10037=DIRECTION('center_axis',(0.,0.,1.));
#10038=DIRECTION('ref_axis',(1.,0.,0.));
#10039=DIRECTION('',(1.,0.,0.));
#10040=DIRECTION('',(0.,-1.,0.));
#10041=DIRECTION('',(-1.,0.,0.));
#10042=DIRECTION('',(0.,1.,0.));
#10043=DIRECTION('center_axis',(0.,1.,0.));
#10044=DIRECTION('ref_axis',(-1.,0.,0.));
#10045=DIRECTION('',(0.,0.,1.));
#10046=DIRECTION('',(-1.,0.,0.));
#10047=DIRECTION('',(0.,0.,1.));
#10048=DIRECTION('center_axis',(0.,0.,1.));
#10049=DIRECTION('ref_axis',(1.,0.,0.));
#10050=DIRECTION('',(0.,-1.,0.));
#10051=DIRECTION('',(1.,0.,0.));
#10052=DIRECTION('',(0.,1.,0.));
#10053=DIRECTION('center_axis',(0.,0.,-1.));
#10054=DIRECTION('ref_axis',(1.,0.,0.));
#10055=DIRECTION('center_axis',(-1.,0.,0.));
#10056=DIRECTION('ref_axis',(0.,-1.,0.));
#10057=DIRECTION('',(0.,0.,1.));
#10058=DIRECTION('',(0.,0.707106781186548,0.707106781186548));
#10059=DIRECTION('',(0.,-1.,0.));
#10060=DIRECTION('',(0.,0.707106781186548,-0.707106781186548));
#10061=DIRECTION('',(0.,0.,1.));
#10062=DIRECTION('',(0.,-1.,0.));
#10063=DIRECTION('',(0.,0.,1.));
#10064=DIRECTION('center_axis',(0.,-1.,0.));
#10065=DIRECTION('ref_axis',(1.,0.,0.));
#10066=DIRECTION('',(1.,0.,0.));
#10067=DIRECTION('',(0.,0.,1.));
#10068=DIRECTION('center_axis',(0.,0.,1.));
#10069=DIRECTION('ref_axis',(1.,0.,0.));
#10070=DIRECTION('',(-1.,0.,0.));
#10071=DIRECTION('',(0.,1.,0.));
#10072=DIRECTION('center_axis',(1.,0.,0.));
#10073=DIRECTION('ref_axis',(0.,1.,0.));
#10074=DIRECTION('',(0.,0.,1.));
#10075=DIRECTION('',(0.,-0.707106781186548,0.707106781186548));
#10076=DIRECTION('',(0.,1.,0.));
#10077=DIRECTION('',(0.,-0.707106781186548,-0.707106781186548));
#10078=DIRECTION('',(0.,0.,1.));
#10079=DIRECTION('center_axis',(0.,-1.,0.));
#10080=DIRECTION('ref_axis',(1.,0.,0.));
#10081=DIRECTION('',(-1.,0.,0.));
#10082=DIRECTION('center_axis',(0.,-0.707106781186548,-0.707106781186548));
#10083=DIRECTION('ref_axis',(-1.,0.,0.));
#10084=DIRECTION('',(1.,0.,0.));
#10085=DIRECTION('center_axis',(0.,0.707106781186548,0.707106781186548));
#10086=DIRECTION('ref_axis',(0.,0.707106781186547,-0.707106781186547));
#10087=DIRECTION('',(1.,0.,0.));
#10088=DIRECTION('center_axis',(0.,0.,1.));
#10089=DIRECTION('ref_axis',(1.,0.,0.));
#10090=DIRECTION('center_axis',(0.,0.,-1.));
#10091=DIRECTION('ref_axis',(1.,0.,0.));
#10092=DIRECTION('',(0.,0.,1.));
#10093=DIRECTION('center_axis',(0.,0.,-1.));
#10094=DIRECTION('ref_axis',(1.,0.,0.));
#10095=DIRECTION('center_axis',(0.,-0.707106781186548,0.707106781186548));
#10096=DIRECTION('ref_axis',(0.,0.707106781186547,0.707106781186547));
#10097=DIRECTION('center_axis',(0.,0.,-1.));
#10098=DIRECTION('ref_axis',(1.,0.,0.));
#10099=DIRECTION('center_axis',(0.,0.,1.));
#10100=DIRECTION('ref_axis',(1.,0.,0.));
#10101=DIRECTION('',(-1.,0.,0.));
#10102=DIRECTION('center_axis',(0.,0.,1.));
#10103=DIRECTION('ref_axis',(1.,0.,0.));
#10104=DIRECTION('',(-1.,0.,0.));
#10105=DIRECTION('center_axis',(0.,0.707106781186548,-0.707106781186548));
#10106=DIRECTION('ref_axis',(-1.,0.,0.));
#10107=DIRECTION('',(1.,0.,0.));
#10108=DIRECTION('center_axis',(0.,1.,0.));
#10109=DIRECTION('ref_axis',(-1.,0.,0.));
#12254=CARTESIAN_POINT('',(0.,0.,0.));
#12255=CARTESIAN_POINT('Origin',(0.,0.395,0.25));
#12256=CARTESIAN_POINT('',(-0.5,0.3,0.25));
#12257=CARTESIAN_POINT('',(0.5,0.3,0.25));
#12258=CARTESIAN_POINT('',(0.25,0.3,0.25));
#12259=CARTESIAN_POINT('',(-0.5,0.5,0.25));
#12260=CARTESIAN_POINT('',(-0.5,0.5,0.25));
#12261=CARTESIAN_POINT('',(0.5,0.5,0.25));
#12262=CARTESIAN_POINT('',(0.5,0.5,0.25));
#12263=CARTESIAN_POINT('',(0.5,0.29,0.25));
#12264=CARTESIAN_POINT('Origin',(0.5,0.5,0.25));
#12265=CARTESIAN_POINT('',(-0.5,0.5,0.4));
#12266=CARTESIAN_POINT('',(-0.5,0.5,0.25));
#12267=CARTESIAN_POINT('',(0.5,0.5,0.4));
#12268=CARTESIAN_POINT('',(0.5,0.5,0.4));
#12269=CARTESIAN_POINT('',(0.5,0.5,0.25));
#12270=CARTESIAN_POINT('Origin',(0.,0.,0.4));
#12271=CARTESIAN_POINT('',(-0.5,-0.5,0.4));
#12272=CARTESIAN_POINT('',(-0.5,0.5,0.4));
#12273=CARTESIAN_POINT('',(0.5,-0.5,0.4));
#12274=CARTESIAN_POINT('',(-0.5,-0.5,0.4));
#12275=CARTESIAN_POINT('',(0.5,-0.3,0.4));
#12276=CARTESIAN_POINT('',(-0.2117,2.59257727379495E-17,0.4));
#12277=CARTESIAN_POINT('Origin',(0.,0.,0.4));
#12278=CARTESIAN_POINT('Origin',(-0.5,0.3,0.));
#12279=CARTESIAN_POINT('',(-0.5,0.3,0.15));
#12280=CARTESIAN_POINT('',(-0.5,0.3,0.));
#12281=CARTESIAN_POINT('',(-0.5,0.15,0.));
#12282=CARTESIAN_POINT('',(-0.5,0.225,0.075));
#12283=CARTESIAN_POINT('',(-0.5,-0.15,0.));
#12284=CARTESIAN_POINT('',(-0.5,0.3,0.));
#12285=CARTESIAN_POINT('',(-0.5,-0.3,0.15));
#12286=CARTESIAN_POINT('',(-0.5,-0.075,-0.075));
#12287=CARTESIAN_POINT('',(-0.5,-0.3,0.25));
#12288=CARTESIAN_POINT('',(-0.5,-0.3,0.));
#12289=CARTESIAN_POINT('',(-0.5,-0.5,0.25));
#12290=CARTESIAN_POINT('',(-0.5,-0.29,0.25));
#12291=CARTESIAN_POINT('',(-0.5,-0.5,0.25));
#12292=CARTESIAN_POINT('Origin',(-0.5,-0.5,0.25));
#12293=CARTESIAN_POINT('',(0.5,-0.5,0.25));
#12294=CARTESIAN_POINT('',(-0.5,-0.5,0.25));
#12295=CARTESIAN_POINT('',(0.5,-0.5,0.25));
#12296=CARTESIAN_POINT('Origin',(0.,-0.395,0.25));
#12297=CARTESIAN_POINT('',(0.5,-0.3,0.25));
#12298=CARTESIAN_POINT('',(-0.25,-0.3,0.25));
#12299=CARTESIAN_POINT('',(0.5,-0.5,0.25));
#12300=CARTESIAN_POINT('Origin',(0.5,-0.3,0.));
#12301=CARTESIAN_POINT('',(0.5,-0.3,0.15));
#12302=CARTESIAN_POINT('',(0.5,-0.3,0.));
#12303=CARTESIAN_POINT('',(0.5,-0.15,0.));
#12304=CARTESIAN_POINT('',(0.5,-0.225,0.075));
#12305=CARTESIAN_POINT('',(0.5,0.15,0.));
#12306=CARTESIAN_POINT('',(0.5,-0.3,0.));
#12307=CARTESIAN_POINT('',(0.5,0.3,0.15));
#12308=CARTESIAN_POINT('',(0.5,0.075,-0.075));
#12309=CARTESIAN_POINT('',(0.5,0.3,0.));
#12310=CARTESIAN_POINT('Origin',(-0.5,-0.3,0.));
#12311=CARTESIAN_POINT('',(-0.25,-0.3,0.15));
#12312=CARTESIAN_POINT('Origin',(-0.25,-0.225,0.075));
#12313=CARTESIAN_POINT('',(-0.149388386429468,-0.15,0.));
#12314=CARTESIAN_POINT('',(-0.25,-0.15,0.));
#12315=CARTESIAN_POINT('',(0.149388386429468,-0.15,0.));
#12316=CARTESIAN_POINT('Origin',(0.,0.,-0.15));
#12317=CARTESIAN_POINT('',(-0.25,-0.15,0.));
#12318=CARTESIAN_POINT('Origin',(0.,0.,-0.1));
#12319=CARTESIAN_POINT('',(-0.2117,-2.59257727379495E-17,0.));
#12320=CARTESIAN_POINT('Origin',(0.,0.,0.));
#12321=CARTESIAN_POINT('',(-0.2117,-2.59257727379495E-17,-0.1));
#12322=CARTESIAN_POINT('',(-0.149388386429468,0.15,0.));
#12323=CARTESIAN_POINT('Origin',(0.,0.,0.));
#12324=CARTESIAN_POINT('',(0.149388386429468,0.15,0.));
#12325=CARTESIAN_POINT('Origin',(0.,0.,-0.15));
#12326=CARTESIAN_POINT('Origin',(0.,0.,0.));
#12327=CARTESIAN_POINT('Origin',(0.,0.,0.));
#12328=CARTESIAN_POINT('',(0.25,0.15,0.));
#12329=CARTESIAN_POINT('Origin',(0.,0.,0.));
#12330=CARTESIAN_POINT('',(0.25,0.15,0.));
#12331=CARTESIAN_POINT('Origin',(0.25,0.225,0.075));
#12332=CARTESIAN_POINT('',(0.25,0.3,0.15));
#12333=CARTESIAN_POINT('Origin',(0.5,0.3,0.));
#13045=UNCERTAINTY_MEASURE_WITH_UNIT(LENGTH_MEASURE(0.001),#13095,
'DISTANCE_ACCURACY_VALUE',
'Maximum model space distance between geometric entities at asserted c
onnectivities');
#13057=UNCERTAINTY_MEASURE_WITH_UNIT(LENGTH_MEASURE(0.001),#13095,
'DISTANCE_ACCURACY_VALUE',
'Maximum model space distance between geometric entities at asserted c
onnectivities');
#13082=(
GEOMETRIC_REPRESENTATION_CONTEXT(3)
GLOBAL_UNCERTAINTY_ASSIGNED_CONTEXT((#13045))
GLOBAL_UNIT_ASSIGNED_CONTEXT((#13095,#13097,#13098))
REPRESENTATION_CONTEXT('','3D')
);
#13094=(
GEOMETRIC_REPRESENTATION_CONTEXT(3)
GLOBAL_UNCERTAINTY_ASSIGNED_CONTEXT((#13057))
GLOBAL_UNIT_ASSIGNED_CONTEXT((#13095,#13097,#13098))
REPRESENTATION_CONTEXT('','3D')
);
#13095=(
LENGTH_UNIT()
NAMED_UNIT(*)
SI_UNIT(.CENTI.,.METRE.)
);
#13097=(
NAMED_UNIT(*)
PLANE_ANGLE_UNIT()
SI_UNIT($,.RADIAN.)
);
#13098=(
NAMED_UNIT(*)
SI_UNIT($,.STERADIAN.)
SOLID_ANGLE_UNIT()
);
#13123=SHAPE_DEFINITION_REPRESENTATION(#13159,#13273);
#13159=PRODUCT_DEFINITION_SHAPE('',$,#13310);
#13273=SHAPE_REPRESENTATION('',(#8390),#13082);
#13285=PRODUCT_DEFINITION_CONTEXT('part definition',#13395,'design');
#13310=PRODUCT_DEFINITION('Captive slot nut','Captive slot nut',#13346,
#13285);
#13346=PRODUCT_DEFINITION_FORMATION('',$,#13421);
#13395=APPLICATION_CONTEXT(
'Core Data for Automotive Mechanical Design Process');
#13396=PRODUCT_CONTEXT('part definition',#13395,'mechanical');
#13421=PRODUCT('Captive slot nut','Captive slot nut','Captive slot nut',
(#13396));
#13496=COLOUR_RGB('Black',0.12,0.14,0.17);
#13497=FILL_AREA_STYLE_COLOUR('',#13496);
#13498=FILL_AREA_STYLE('',(#13497));
#13499=SURFACE_STYLE_FILL_AREA(#13498);
#13500=SURFACE_SIDE_STYLE('',(#13499));
#13501=SURFACE_STYLE_USAGE(.BOTH.,#13500);
#13502=PRESENTATION_STYLE_ASSIGNMENT((#13501));
ENDSEC;
END-ISO-10303-21;
